ISO-10303-21;
HEADER;
/* Generated by software containing ST-Developer
 * from STEP Tools, Inc. (www.steptools.com) 
 */

FILE_DESCRIPTION(
/* description */ ('Four-bar parallelogram arm'),
/* implementation_level */ '2;1');

FILE_NAME(
/* name */ 'Bearing cap (5).step',
/* time_stamp */ '2026-10-28T03:24:55-07:00',
/* author */ (''),
/* organization */ (''),
/* preprocessor_version */ 'ST-DEVELOPER v20.2',
/* originating_system */ 'Autodesk Translation Framework v15.17.0.0',
/* authorisation */ '');

FILE_SCHEMA (('AUTOMOTIVE_DESIGN { 1 0 10303 214 3 1 1 }'));
ENDSEC;

DATA;
#10=MECHANICAL_DESIGN_GEOMETRIC_PRESENTATION_REPRESENTATION('',(#650),#14512);
#550=SHAPE_REPRESENTATION_RELATIONSHIP('SRR','None',#14773,#600);
#600=ADVANCED_BREP_SHAPE_REPRESENTATION('',(#707),#14488);
#650=STYLED_ITEM('',(#15087),#707);
#707=MANIFOLD_SOLID_BREP('Body1',#7355);
#905=FACE_BOUND('',#2029,.T.);
#906=FACE_BOUND('',#2030,.T.);
#907=FACE_BOUND('',#2031,.T.);
#908=FACE_BOUND('',#2032,.T.);
#909=FACE_BOUND('',#2033,.T.);
#910=FACE_BOUND('',#2035,.T.);
#911=FACE_BOUND('',#2036,.T.);
#912=FACE_BOUND('',#2037,.T.);
#913=FACE_BOUND('',#2038,.T.);
#914=FACE_BOUND('',#2039,.T.);
#1119=PLANE('',#8453);
#1120=PLANE('',#8454);
#1432=FACE_OUTER_BOUND('',#2022,.T.);
#1433=FACE_OUTER_BOUND('',#2023,.T.);
#1434=FACE_OUTER_BOUND('',#2024,.T.);
#1435=FACE_OUTER_BOUND('',#2025,.T.);
#1436=FACE_OUTER_BOUND('',#2026,.T.);
#1437=FACE_OUTER_BOUND('',#2027,.T.);
#1438=FACE_OUTER_BOUND('',#2028,.T.);
#1439=FACE_OUTER_BOUND('',#2034,.T.);
#2022=EDGE_LOOP('',(#5964,#5965,#5966,#5967));
#2023=EDGE_LOOP('',(#5968,#5969,#5970,#5971));
#2024=EDGE_LOOP('',(#5972,#5973,#5974,#5975));
#2025=EDGE_LOOP('',(#5976,#5977,#5978,#5979));
#2026=EDGE_LOOP('',(#5980,#5981,#5982,#5983));
#2027=EDGE_LOOP('',(#5984,#5985,#5986,#5987));
#2028=EDGE_LOOP('',(#5988));
#2029=EDGE_LOOP('',(#5989));
#2030=EDGE_LOOP('',(#5990));
#2031=EDGE_LOOP('',(#5991));
#2032=EDGE_LOOP('',(#5992));
#2033=EDGE_LOOP('',(#5993));
#2034=EDGE_LOOP('',(#5994));
#2035=EDGE_LOOP('',(#5995));
#2036=EDGE_LOOP('',(#5996));
#2037=EDGE_LOOP('',(#5997));
#2038=EDGE_LOOP('',(#5998));
#2039=EDGE_LOOP('',(#5999));
#2560=LINE('',#13109,#2954);
#2561=LINE('',#13115,#2955);
#2562=LINE('',#13121,#2956);
#2563=LINE('',#13127,#2957);
#2564=LINE('',#13133,#2958);
#2565=LINE('',#13139,#2959);
#2954=VECTOR('',#10216,0.225);
#2955=VECTOR('',#10223,0.225);
#2956=VECTOR('',#10230,0.225);
#2957=VECTOR('',#10237,0.225);
#2958=VECTOR('',#10244,1.02);
#2959=VECTOR('',#10251,2.2);
#3334=CIRCLE('',#8436,0.225);
#3335=CIRCLE('',#8437,0.225);
#3336=CIRCLE('',#8439,0.225);
#3337=CIRCLE('',#8440,0.225);
#3338=CIRCLE('',#8442,0.225);
#3339=CIRCLE('',#8443,0.225);
#3340=CIRCLE('',#8445,0.225);
#3341=CIRCLE('',#8446,0.225);
#3342=CIRCLE('',#8448,1.02);
#3343=CIRCLE('',#8449,1.02);
#3344=CIRCLE('',#8451,2.2);
#3345=CIRCLE('',#8452,2.2);
#3868=VERTEX_POINT('',#13106);
#3869=VERTEX_POINT('',#13108);
#3870=VERTEX_POINT('',#13112);
#3871=VERTEX_POINT('',#13114);
#3872=VERTEX_POINT('',#13118);
#3873=VERTEX_POINT('',#13120);
#3874=VERTEX_POINT('',#13124);
#3875=VERTEX_POINT('',#13126);
#3876=VERTEX_POINT('',#13130);
#3877=VERTEX_POINT('',#13132);
#3878=VERTEX_POINT('',#13136);
#3879=VERTEX_POINT('',#13138);
#4613=EDGE_CURVE('',#3868,#3868,#3334,.T.);
#4614=EDGE_CURVE('',#3868,#3869,#2560,.T.);
#4615=EDGE_CURVE('',#3869,#3869,#3335,.T.);
#4616=EDGE_CURVE('',#3870,#3870,#3336,.T.);
#4617=EDGE_CURVE('',#3870,#3871,#2561,.T.);
#4618=EDGE_CURVE('',#3871,#3871,#3337,.T.);
#4619=EDGE_CURVE('',#3872,#3872,#3338,.T.);
#4620=EDGE_CURVE('',#3872,#3873,#2562,.T.);
#4621=EDGE_CURVE('',#3873,#3873,#3339,.T.);
#4622=EDGE_CURVE('',#3874,#3874,#3340,.T.);
#4623=EDGE_CURVE('',#3874,#3875,#2563,.T.);
#4624=EDGE_CURVE('',#3875,#3875,#3341,.T.);
#4625=EDGE_CURVE('',#3876,#3876,#3342,.T.);
#4626=EDGE_CURVE('',#3876,#3877,#2564,.T.);
#4627=EDGE_CURVE('',#3877,#3877,#3343,.T.);
#4628=EDGE_CURVE('',#3878,#3878,#3344,.T.);
#4629=EDGE_CURVE('',#3878,#3879,#2565,.T.);
#4630=EDGE_CURVE('',#3879,#3879,#3345,.T.);
#5964=ORIENTED_EDGE('',*,*,#4613,.F.);
#5965=ORIENTED_EDGE('',*,*,#4614,.T.);
#5966=ORIENTED_EDGE('',*,*,#4615,.F.);
#5967=ORIENTED_EDGE('',*,*,#4614,.F.);
#5968=ORIENTED_EDGE('',*,*,#4616,.F.);
#5969=ORIENTED_EDGE('',*,*,#4617,.T.);
#5970=ORIENTED_EDGE('',*,*,#4618,.F.);
#5971=ORIENTED_EDGE('',*,*,#4617,.F.);
#5972=ORIENTED_EDGE('',*,*,#4619,.F.);
#5973=ORIENTED_EDGE('',*,*,#4620,.T.);
#5974=ORIENTED_EDGE('',*,*,#4621,.F.);
#5975=ORIENTED_EDGE('',*,*,#4620,.F.);
#5976=ORIENTED_EDGE('',*,*,#4622,.F.);
#5977=ORIENTED_EDGE('',*,*,#4623,.T.);
#5978=ORIENTED_EDGE('',*,*,#4624,.F.);
#5979=ORIENTED_EDGE('',*,*,#4623,.F.);
#5980=ORIENTED_EDGE('',*,*,#4625,.F.);
#5981=ORIENTED_EDGE('',*,*,#4626,.T.);
#5982=ORIENTED_EDGE('',*,*,#4627,.T.);
#5983=ORIENTED_EDGE('',*,*,#4626,.F.);
#5984=ORIENTED_EDGE('',*,*,#4628,.F.);
#5985=ORIENTED_EDGE('',*,*,#4629,.T.);
#5986=ORIENTED_EDGE('',*,*,#4630,.T.);
#5987=ORIENTED_EDGE('',*,*,#4629,.F.);
#5988=ORIENTED_EDGE('',*,*,#4628,.T.);
#5989=ORIENTED_EDGE('',*,*,#4625,.T.);
#5990=ORIENTED_EDGE('',*,*,#4624,.T.);
#5991=ORIENTED_EDGE('',*,*,#4621,.T.);
#5992=ORIENTED_EDGE('',*,*,#4618,.T.);
#5993=ORIENTED_EDGE('',*,*,#4615,.T.);
#5994=ORIENTED_EDGE('',*,*,#4630,.F.);
#5995=ORIENTED_EDGE('',*,*,#4627,.F.);
#5996=ORIENTED_EDGE('',*,*,#4622,.T.);
#5997=ORIENTED_EDGE('',*,*,#4619,.T.);
#5998=ORIENTED_EDGE('',*,*,#4616,.T.);
#5999=ORIENTED_EDGE('',*,*,#4613,.T.);
#6828=CYLINDRICAL_SURFACE('',#8435,0.225);
#6829=CYLINDRICAL_SURFACE('',#8438,0.225);
#6830=CYLINDRICAL_SURFACE('',#8441,0.225);
#6831=CYLINDRICAL_SURFACE('',#8444,0.225);
#6832=CYLINDRICAL_SURFACE('',#8447,1.02);
#6833=CYLINDRICAL_SURFACE('',#8450,2.2);
#7137=ADVANCED_FACE('',(#1432),#6828,.F.);
#7138=ADVANCED_FACE('',(#1433),#6829,.F.);
#7139=ADVANCED_FACE('',(#1434),#6830,.F.);
#7140=ADVANCED_FACE('',(#1435),#6831,.F.);
#7141=ADVANCED_FACE('',(#1436),#6832,.F.);
#7142=ADVANCED_FACE('',(#1437),#6833,.T.);
#7143=ADVANCED_FACE('',(#1438,#905,#906,#907,#908,#909),#1119,.T.);
#7144=ADVANCED_FACE('',(#1439,#910,#911,#912,#913,#914),#1120,.F.);
#7355=CLOSED_SHELL('',(#7137,#7138,#7139,#7140,#7141,#7142,#7143,#7144));
#8434=AXIS2_PLACEMENT_3D('',#13104,#10210,#10211);
#8435=AXIS2_PLACEMENT_3D('',#13105,#10212,#10213);
#8436=AXIS2_PLACEMENT_3D('',#13107,#10214,#10215);
#8437=AXIS2_PLACEMENT_3D('',#13110,#10217,#10218);
#8438=AXIS2_PLACEMENT_3D('',#13111,#10219,#10220);
#8439=AXIS2_PLACEMENT_3D('',#13113,#10221,#10222);
#8440=AXIS2_PLACEMENT_3D('',#13116,#10224,#10225);
#8441=AXIS2_PLACEMENT_3D('',#13117,#10226,#10227);
#8442=AXIS2_PLACEMENT_3D('',#13119,#10228,#10229);
#8443=AXIS2_PLACEMENT_3D('',#13122,#10231,#10232);
#8444=AXIS2_PLACEMENT_3D('',#13123,#10233,#10234);
#8445=AXIS2_PLACEMENT_3D('',#13125,#10235,#10236);
#8446=AXIS2_PLACEMENT_3D('',#13128,#10238,#10239);
#8447=AXIS2_PLACEMENT_3D('',#13129,#10240,#10241);
#8448=AXIS2_PLACEMENT_3D('',#13131,#10242,#10243);
#8449=AXIS2_PLACEMENT_3D('',#13134,#10245,#10246);
#8450=AXIS2_PLACEMENT_3D('',#13135,#10247,#10248);
#8451=AXIS2_PLACEMENT_3D('',#13137,#10249,#10250);
#8452=AXIS2_PLACEMENT_3D('',#13140,#10252,#10253);
#8453=AXIS2_PLACEMENT_3D('',#13141,#10254,#10255);
#8454=AXIS2_PLACEMENT_3D('',#13142,#10256,#10257);
#10210=DIRECTION('axis',(0.,0.,1.));
#10211=DIRECTION('refdir',(1.,0.,0.));
#10212=DIRECTION('center_axis',(0.,1.,0.));
#10213=DIRECTION('ref_axis',(1.,0.,0.));
#10214=DIRECTION('center_axis',(0.,1.,0.));
#10215=DIRECTION('ref_axis',(1.,0.,0.));
#10216=DIRECTION('',(0.,1.,0.));
#10217=DIRECTION('center_axis',(0.,-1.,0.));
#10218=DIRECTION('ref_axis',(1.,0.,0.));
#10219=DIRECTION('center_axis',(0.,1.,0.));
#10220=DIRECTION('ref_axis',(1.,0.,0.));
#10221=DIRECTION('center_axis',(0.,1.,0.));
#10222=DIRECTION('ref_axis',(1.,0.,0.));
#10223=DIRECTION('',(0.,1.,0.));
#10224=DIRECTION('center_axis',(0.,-1.,0.));
#10225=DIRECTION('ref_axis',(1.,0.,0.));
#10226=DIRECTION('center_axis',(0.,1.,0.));
#10227=DIRECTION('ref_axis',(1.,0.,0.));
#10228=DIRECTION('center_axis',(0.,1.,0.));
#10229=DIRECTION('ref_axis',(1.,0.,0.));
#10230=DIRECTION('',(0.,1.,0.));
#10231=DIRECTION('center_axis',(0.,-1.,0.));
#10232=DIRECTION('ref_axis',(1.,0.,0.));
#10233=DIRECTION('center_axis',(0.,1.,0.));
#10234=DIRECTION('ref_axis',(1.,0.,0.));
#10235=DIRECTION('center_axis',(0.,1.,0.));
#10236=DIRECTION('ref_axis',(1.,0.,0.));
#10237=DIRECTION('',(0.,1.,0.));
#10238=DIRECTION('center_axis',(0.,-1.,0.));
#10239=DIRECTION('ref_axis',(1.,0.,0.));
#10240=DIRECTION('center_axis',(0.,1.,0.));
#10241=DIRECTION('ref_axis',(1.,0.,0.));
#10242=DIRECTION('center_axis',(0.,-1.,0.));
#10243=DIRECTION('ref_axis',(1.,0.,0.));
#10244=DIRECTION('',(0.,-1.,0.));
#10245=DIRECTION('center_axis',(0.,-1.,0.));
#10246=DIRECTION('ref_axis',(1.,0.,0.));
#10247=DIRECTION('center_axis',(0.,1.,0.));
#10248=DIRECTION('ref_axis',(1.,0.,0.));
#10249=DIRECTION('center_axis',(0.,1.,0.));
#10250=DIRECTION('ref_axis',(1.,0.,0.));
#10251=DIRECTION('',(0.,-1.,0.));
#10252=DIRECTION('center_axis',(0.,1.,0.));
#10253=DIRECTION('ref_axis',(1.,0.,0.));
#10254=DIRECTION('center_axis',(0.,1.,0.));
#10255=DIRECTION('ref_axis',(1.,0.,0.));
#10256=DIRECTION('center_axis',(0.,1.,0.));
#10257=DIRECTION('ref_axis',(1.,0.,0.));
#13104=CARTESIAN_POINT('',(0.,0.,0.));
#13105=CARTESIAN_POINT('Origin',(-1.23743686707646,0.95,12.7625631329235));
#13106=CARTESIAN_POINT('',(-1.46243686707646,1.05,12.7625631329235));
#13107=CARTESIAN_POINT('Origin',(-1.23743686707646,1.05,12.7625631329235));
#13108=CARTESIAN_POINT('',(-1.46243686707646,1.4,12.7625631329235));
#13109=CARTESIAN_POINT('',(-1.46243686707646,0.95,12.7625631329235));
#13110=CARTESIAN_POINT('Origin',(-1.23743686707646,1.4,12.7625631329235));
#13111=CARTESIAN_POINT('Origin',(-1.23743686707646,0.95,15.2374368670765));
#13112=CARTESIAN_POINT('',(-1.46243686707646,1.05,15.2374368670765));
#13113=CARTESIAN_POINT('Origin',(-1.23743686707646,1.05,15.2374368670765));
#13114=CARTESIAN_POINT('',(-1.46243686707646,1.4,15.2374368670765));
#13115=CARTESIAN_POINT('',(-1.46243686707646,0.95,15.2374368670765));
#13116=CARTESIAN_POINT('Origin',(-1.23743686707646,1.4,15.2374368670765));
#13117=CARTESIAN_POINT('Origin',(1.23743686707646,0.95,15.2374368670765));
#13118=CARTESIAN_POINT('',(1.01243686707646,1.05,15.2374368670765));
#13119=CARTESIAN_POINT('Origin',(1.23743686707646,1.05,15.2374368670765));
#13120=CARTESIAN_POINT('',(1.01243686707646,1.4,15.2374368670765));
#13121=CARTESIAN_POINT('',(1.01243686707646,0.95,15.2374368670765));
#13122=CARTESIAN_POINT('Origin',(1.23743686707646,1.4,15.2374368670765));
#13123=CARTESIAN_POINT('Origin',(1.23743686707646,0.95,12.7625631329235));
#13124=CARTESIAN_POINT('',(1.01243686707646,1.05,12.7625631329235));
#13125=CARTESIAN_POINT('Origin',(1.23743686707646,1.05,12.7625631329235));
#13126=CARTESIAN_POINT('',(1.01243686707646,1.4,12.7625631329235));
#13127=CARTESIAN_POINT('',(1.01243686707646,0.95,12.7625631329235));
#13128=CARTESIAN_POINT('Origin',(1.23743686707646,1.4,12.7625631329235));
#13129=CARTESIAN_POINT('Origin',(0.,1.05,14.));
#13130=CARTESIAN_POINT('',(-1.02,1.4,14.));
#13131=CARTESIAN_POINT('Origin',(0.,1.4,14.));
#13132=CARTESIAN_POINT('',(-1.02,1.05,14.));
#13133=CARTESIAN_POINT('',(-1.02,1.05,14.));
#13134=CARTESIAN_POINT('Origin',(0.,1.05,14.));
#13135=CARTESIAN_POINT('Origin',(0.,1.05,14.));
#13136=CARTESIAN_POINT('',(-2.2,1.4,14.));
#13137=CARTESIAN_POINT('Origin',(0.,1.4,14.));
#13138=CARTESIAN_POINT('',(-2.2,1.05,14.));
#13139=CARTESIAN_POINT('',(-2.2,1.05,14.));
#13140=CARTESIAN_POINT('Origin',(0.,1.05,14.));
#13141=CARTESIAN_POINT('Origin',(0.,1.4,14.));
#13142=CARTESIAN_POINT('Origin',(0.,1.05,14.));
#14431=UNCERTAINTY_MEASURE_WITH_UNIT(LENGTH_MEASURE(0.001),#14513,
'DISTANCE_ACCURACY_VALUE',
'Maximum model space distance between geometric entities at asserted c
onnectivities');
#14455=UNCERTAINTY_MEASURE_WITH_UNIT(LENGTH_MEASURE(0.001),#14513,
'DISTANCE_ACCURACY_VALUE',
'Maximum model space distance between geometric entities at asserted c
onnectivities');
#14488=(
GEOMETRIC_REPRESENTATION_CONTEXT(3)
GLOBAL_UNCERTAINTY_ASSIGNED_CONTEXT((#14431))
GLOBAL_UNIT_ASSIGNED_CONTEXT((#14513,#14515,#14516))
REPRESENTATION_CONTEXT('','3D')
);
#14512=(
GEOMETRIC_REPRESENTATION_CONTEXT(3)
GLOBAL_UNCERTAINTY_ASSIGNED_CONTEXT((#14455))
GLOBAL_UNIT_ASSIGNED_CONTEXT((#14513,#14515,#14516))
REPRESENTATION_CONTEXT('','3D')
);
#14513=(
LENGTH_UNIT()
NAMED_UNIT(*)
SI_UNIT(.CENTI.,.METRE.)
);
#14515=(
NAMED_UNIT(*)
PLANE_ANGLE_UNIT()
SI_UNIT($,.RADIAN.)
);
#14516=(
NAMED_UNIT(*)
SI_UNIT($,.STERADIAN.)
SOLID_ANGLE_UNIT()
);
#14549=SHAPE_DEFINITION_REPRESENTATION(#14605,#14773);
#14605=PRODUCT_DEFINITION_SHAPE('',$,#14830);
#14773=SHAPE_REPRESENTATION('',(#8434),#14488);
#14797=PRODUCT_DEFINITION_CONTEXT('part definition',#14967,'design');
#14830=PRODUCT_DEFINITION('Bearing cap (5)','Bearing cap (5)',#14886,#14797);
#14886=PRODUCT_DEFINITION_FORMATION('',$,#15001);
#14967=APPLICATION_CONTEXT(
'Core Data for Automotive Mechanical Design Process');
#14968=PRODUCT_CONTEXT('part definition',#14967,'mechanical');
#15001=PRODUCT('Bearing cap (5)','Bearing cap (5)','Bearing cap (5)',(#14968));
#15081=COLOUR_RGB('Grey',0.48,0.52,0.57);
#15082=FILL_AREA_STYLE_COLOUR('',#15081);
#15083=FILL_AREA_STYLE('',(#15082));
#15084=SURFACE_STYLE_FILL_AREA(#15083);
#15085=SURFACE_SIDE_STYLE('',(#15084));
#15086=SURFACE_STYLE_USAGE(.BOTH.,#15085);
#15087=PRESENTATION_STYLE_ASSIGNMENT((#15086));
ENDSEC;
END-ISO-10303-21;
